ISO-10303-21;
HEADER;
/* Generated by software containing ST-Developer
 * from STEP Tools, Inc. (www.steptools.com) 
 */

FILE_DESCRIPTION(
/* description */ ('Hand-crank flanged shaft unit'),
/* implementation_level */ '2;1');

FILE_NAME(
/* name */ 'Flat Washer - M8.step',
/* time_stamp */ '2026-10-27T18:35:45-07:00',
/* author */ (''),
/* organization */ (''),
/* preprocessor_version */ 'ST-DEVELOPER v20.2',
/* originating_system */ 'Autodesk Translation Framework v15.17.0.0',
/* authorisation */ '');

FILE_SCHEMA (('AUTOMOTIVE_DESIGN { 1 0 10303 214 3 1 1 }'));
ENDSEC;

DATA;
#10=MECHANICAL_DESIGN_GEOMETRIC_PRESENTATION_REPRESENTATION('',(#291),#6805);
#250=SHAPE_REPRESENTATION_RELATIONSHIP('SRR','None',#6912,#270);
#270=ADVANCED_BREP_SHAPE_REPRESENTATION('',(#312),#6795);
#291=STYLED_ITEM('',(#7098),#312);
#312=MANIFOLD_SOLID_BREP('Body1',#3332);
#391=FACE_BOUND('',#872,.T.);
#392=FACE_BOUND('',#874,.T.);
#459=PLANE('',#3750);
#460=PLANE('',#3751);
#610=FACE_OUTER_BOUND('',#869,.T.);
#611=FACE_OUTER_BOUND('',#870,.T.);
#612=FACE_OUTER_BOUND('',#871,.T.);
#613=FACE_OUTER_BOUND('',#873,.T.);
#869=EDGE_LOOP('',(#2667,#2668,#2669,#2670));
#870=EDGE_LOOP('',(#2671,#2672,#2673,#2674));
#871=EDGE_LOOP('',(#2675));
#872=EDGE_LOOP('',(#2676));
#873=EDGE_LOOP('',(#2677));
#874=EDGE_LOOP('',(#2678));
#1085=LINE('',#5810,#1313);
#1086=LINE('',#5816,#1314);
#1313=VECTOR('',#4428,0.42);
#1314=VECTOR('',#4435,0.8);
#1517=CIRCLE('',#3745,0.42);
#1518=CIRCLE('',#3746,0.42);
#1519=CIRCLE('',#3748,0.8);
#1520=CIRCLE('',#3749,0.8);
#1715=VERTEX_POINT('',#5807);
#1716=VERTEX_POINT('',#5809);
#1717=VERTEX_POINT('',#5813);
#1718=VERTEX_POINT('',#5815);
#2051=EDGE_CURVE('',#1715,#1715,#1517,.T.);
#2052=EDGE_CURVE('',#1715,#1716,#1085,.T.);
#2053=EDGE_CURVE('',#1716,#1716,#1518,.T.);
#2054=EDGE_CURVE('',#1717,#1717,#1519,.T.);
#2055=EDGE_CURVE('',#1717,#1718,#1086,.T.);
#2056=EDGE_CURVE('',#1718,#1718,#1520,.T.);
#2667=ORIENTED_EDGE('',*,*,#2051,.F.);
#2668=ORIENTED_EDGE('',*,*,#2052,.T.);
#2669=ORIENTED_EDGE('',*,*,#2053,.T.);
#2670=ORIENTED_EDGE('',*,*,#2052,.F.);
#2671=ORIENTED_EDGE('',*,*,#2054,.F.);
#2672=ORIENTED_EDGE('',*,*,#2055,.T.);
#2673=ORIENTED_EDGE('',*,*,#2056,.T.);
#2674=ORIENTED_EDGE('',*,*,#2055,.F.);
#2675=ORIENTED_EDGE('',*,*,#2054,.T.);
#2676=ORIENTED_EDGE('',*,*,#2051,.T.);
#2677=ORIENTED_EDGE('',*,*,#2056,.F.);
#2678=ORIENTED_EDGE('',*,*,#2053,.F.);
#3111=CYLINDRICAL_SURFACE('',#3744,0.42);
#3112=CYLINDRICAL_SURFACE('',#3747,0.8);
#3227=ADVANCED_FACE('',(#610),#3111,.F.);
#3228=ADVANCED_FACE('',(#611),#3112,.T.);
#3229=ADVANCED_FACE('',(#612,#391),#459,.T.);
#3230=ADVANCED_FACE('',(#613,#392),#460,.F.);
#3332=CLOSED_SHELL('',(#3227,#3228,#3229,#3230));
#3743=AXIS2_PLACEMENT_3D('',#5805,#4422,#4423);
#3744=AXIS2_PLACEMENT_3D('',#5806,#4424,#4425);
#3745=AXIS2_PLACEMENT_3D('',#5808,#4426,#4427);
#3746=AXIS2_PLACEMENT_3D('',#5811,#4429,#4430);
#3747=AXIS2_PLACEMENT_3D('',#5812,#4431,#4432);
#3748=AXIS2_PLACEMENT_3D('',#5814,#4433,#4434);
#3749=AXIS2_PLACEMENT_3D('',#5817,#4436,#4437);
#3750=AXIS2_PLACEMENT_3D('',#5818,#4438,#4439);
#3751=AXIS2_PLACEMENT_3D('',#5819,#4440,#4441);
#4422=DIRECTION('axis',(0.,0.,1.));
#4423=DIRECTION('refdir',(1.,0.,0.));
#4424=DIRECTION('center_axis',(0.,1.,0.));
#4425=DIRECTION('ref_axis',(1.,0.,0.));
#4426=DIRECTION('center_axis',(0.,-1.,0.));
#4427=DIRECTION('ref_axis',(1.,0.,0.));
#4428=DIRECTION('',(0.,-1.,0.));
#4429=DIRECTION('center_axis',(0.,-1.,0.));
#4430=DIRECTION('ref_axis',(1.,0.,0.));
#4431=DIRECTION('center_axis',(0.,1.,0.));
#4432=DIRECTION('ref_axis',(1.,0.,0.));
#4433=DIRECTION('center_axis',(0.,1.,0.));
#4434=DIRECTION('ref_axis',(1.,0.,0.));
#4435=DIRECTION('',(0.,-1.,0.));
#4436=DIRECTION('center_axis',(0.,1.,0.));
#4437=DIRECTION('ref_axis',(1.,0.,0.));
#4438=DIRECTION('center_axis',(0.,1.,0.));
#4439=DIRECTION('ref_axis',(1.,0.,0.));
#4440=DIRECTION('center_axis',(0.,1.,0.));
#4441=DIRECTION('ref_axis',(1.,0.,0.));
#5805=CARTESIAN_POINT('',(0.,0.,0.));
#5806=CARTESIAN_POINT('Origin',(0.,0.,0.));
#5807=CARTESIAN_POINT('',(-0.42,0.16,5.14351655641888E-17));
#5808=CARTESIAN_POINT('Origin',(0.,0.16,0.));
#5809=CARTESIAN_POINT('',(-0.42,0.,5.14351655641888E-17));
#5810=CARTESIAN_POINT('',(-0.42,0.,5.14351655641888E-17));
#5811=CARTESIAN_POINT('Origin',(0.,0.,0.));
#5812=CARTESIAN_POINT('Origin',(0.,0.,0.));
#5813=CARTESIAN_POINT('',(-0.8,0.16,9.79717439317883E-17));
#5814=CARTESIAN_POINT('Origin',(0.,0.16,0.));
#5815=CARTESIAN_POINT('',(-0.8,0.,9.79717439317883E-17));
#5816=CARTESIAN_POINT('',(-0.8,0.,9.79717439317883E-17));
#5817=CARTESIAN_POINT('Origin',(0.,0.,0.));
#5818=CARTESIAN_POINT('Origin',(0.,0.16,0.));
#5819=CARTESIAN_POINT('Origin',(0.,0.,0.));
#6770=UNCERTAINTY_MEASURE_WITH_UNIT(LENGTH_MEASURE(0.001),#6806,
'DISTANCE_ACCURACY_VALUE',
'Maximum model space distance between geometric entities at asserted c
onnectivities');
#6780=UNCERTAINTY_MEASURE_WITH_UNIT(LENGTH_MEASURE(0.001),#6806,
'DISTANCE_ACCURACY_VALUE',
'Maximum model space distance between geometric entities at asserted c
onnectivities');
#6795=(
GEOMETRIC_REPRESENTATION_CONTEXT(3)
GLOBAL_UNCERTAINTY_ASSIGNED_CONTEXT((#6770))
GLOBAL_UNIT_ASSIGNED_CONTEXT((#6806,#6808,#6809))
REPRESENTATION_CONTEXT('','3D')
);
#6805=(
GEOMETRIC_REPRESENTATION_CONTEXT(3)
GLOBAL_UNCERTAINTY_ASSIGNED_CONTEXT((#6780))
GLOBAL_UNIT_ASSIGNED_CONTEXT((#6806,#6808,#6809))
REPRESENTATION_CONTEXT('','3D')
);
#6806=(
LENGTH_UNIT()
NAMED_UNIT(*)
SI_UNIT(.CENTI.,.METRE.)
);
#6808=(
NAMED_UNIT(*)
PLANE_ANGLE_UNIT()
SI_UNIT($,.RADIAN.)
);
#6809=(
NAMED_UNIT(*)
SI_UNIT($,.STERADIAN.)
SOLID_ANGLE_UNIT()
);
#6824=SHAPE_DEFINITION_REPRESENTATION(#6850,#6912);
#6850=PRODUCT_DEFINITION_SHAPE('',$,#6937);
#6912=SHAPE_REPRESENTATION('',(#3743),#6795);
#6922=PRODUCT_DEFINITION_CONTEXT('part definition',#6996,'design');
#6937=PRODUCT_DEFINITION('Flat Washer - M8','Flat Washer - M8',#6961,#6922);
#6961=PRODUCT_DEFINITION_FORMATION('',$,#7012);
#6996=APPLICATION_CONTEXT(
'Core Data for Automotive Mechanical Design Process');
#6997=PRODUCT_CONTEXT('part definition',#6996,'mechanical');
#7012=PRODUCT('Flat Washer - M8','Flat Washer - M8','Flat Washer - M8',
(#6997));
#7092=COLOUR_RGB('Black',0.12,0.14,0.17);
#7093=FILL_AREA_STYLE_COLOUR('',#7092);
#7094=FILL_AREA_STYLE('',(#7093));
#7095=SURFACE_STYLE_FILL_AREA(#7094);
#7096=SURFACE_SIDE_STYLE('',(#7095));
#7097=SURFACE_STYLE_USAGE(.BOTH.,#7096);
#7098=PRESENTATION_STYLE_ASSIGNMENT((#7097));
ENDSEC;
END-ISO-10303-21;
